ISO-10303-21;
HEADER;
/* Generated by software containing ST-Developer
 * from STEP Tools, Inc. (www.steptools.com) 
 */

FILE_DESCRIPTION(
/* description */ ('Cylinder foot and clevis mount kit'),
/* implementation_level */ '2;1');

FILE_NAME(
/* name */ 'Hex Nut - M5.step',
/* time_stamp */ '2026-10-27T20:10:43-07:00',
/* author */ (''),
/* organization */ (''),
/* preprocessor_version */ 'ST-DEVELOPER v20.2',
/* originating_system */ 'Autodesk Translation Framework v15.17.0.0',
/* authorisation */ '');

FILE_SCHEMA (('AUTOMOTIVE_DESIGN { 1 0 10303 214 3 1 1 }'));
ENDSEC;

DATA;
#10=MECHANICAL_DESIGN_GEOMETRIC_PRESENTATION_REPRESENTATION('',(#356),#9102);
#19=(
BOUNDED_CURVE()
B_SPLINE_CURVE(2,(#8429,#8430,#8431),.UNSPECIFIED.,.F.,.F.)
B_SPLINE_CURVE_WITH_KNOTS((3,3),(0.140651836354967,0.670383167684795),
 .UNSPECIFIED.)
CURVE()
GEOMETRIC_REPRESENTATION_ITEM()
RATIONAL_B_SPLINE_CURVE((1.11602540378444,1.28867513459481,1.11602540378444))
REPRESENTATION_ITEM('')
);
#20=(
BOUNDED_CURVE()
B_SPLINE_CURVE(2,(#8433,#8434,#8435),.UNSPECIFIED.,.F.,.F.)
B_SPLINE_CURVE_WITH_KNOTS((3,3),(0.140651836354967,0.670383167684795),
 .UNSPECIFIED.)
CURVE()
GEOMETRIC_REPRESENTATION_ITEM()
RATIONAL_B_SPLINE_CURVE((1.11602540378444,1.28867513459481,1.11602540378444))
REPRESENTATION_ITEM('')
);
#21=(
BOUNDED_CURVE()
B_SPLINE_CURVE(2,(#8440,#8441,#8442),.UNSPECIFIED.,.F.,.F.)
B_SPLINE_CURVE_WITH_KNOTS((3,3),(0.140651836354967,0.670383167684795),
 .UNSPECIFIED.)
CURVE()
GEOMETRIC_REPRESENTATION_ITEM()
RATIONAL_B_SPLINE_CURVE((1.11602540378444,1.28867513459481,1.11602540378444))
REPRESENTATION_ITEM('')
);
#22=(
BOUNDED_CURVE()
B_SPLINE_CURVE(2,(#8444,#8445,#8446),.UNSPECIFIED.,.F.,.F.)
B_SPLINE_CURVE_WITH_KNOTS((3,3),(0.140651836354967,0.670383167684795),
 .UNSPECIFIED.)
CURVE()
GEOMETRIC_REPRESENTATION_ITEM()
RATIONAL_B_SPLINE_CURVE((1.11602540378444,1.28867513459481,1.11602540378444))
REPRESENTATION_ITEM('')
);
#23=(
BOUNDED_CURVE()
B_SPLINE_CURVE(2,(#8448,#8449,#8450),.UNSPECIFIED.,.F.,.F.)
B_SPLINE_CURVE_WITH_KNOTS((3,3),(0.140651836354967,0.670383167684795),
 .UNSPECIFIED.)
CURVE()
GEOMETRIC_REPRESENTATION_ITEM()
RATIONAL_B_SPLINE_CURVE((1.11602540378444,1.28867513459481,1.11602540378444))
REPRESENTATION_ITEM('')
);
#24=(
BOUNDED_CURVE()
B_SPLINE_CURVE(2,(#8451,#8452,#8453),.UNSPECIFIED.,.F.,.F.)
B_SPLINE_CURVE_WITH_KNOTS((3,3),(0.140651836354967,0.670383167684795),
 .UNSPECIFIED.)
CURVE()
GEOMETRIC_REPRESENTATION_ITEM()
RATIONAL_B_SPLINE_CURVE((1.11602540378444,1.28867513459481,1.11602540378444))
REPRESENTATION_ITEM('')
);
#25=(
BOUNDED_CURVE()
B_SPLINE_CURVE(2,(#8460,#8461,#8462),.UNSPECIFIED.,.F.,.F.)
B_SPLINE_CURVE_WITH_KNOTS((3,3),(0.140651836354967,0.670383167684795),
 .UNSPECIFIED.)
CURVE()
GEOMETRIC_REPRESENTATION_ITEM()
RATIONAL_B_SPLINE_CURVE((1.11602540378444,1.28867513459481,1.11602540378444))
REPRESENTATION_ITEM('')
);
#26=(
BOUNDED_CURVE()
B_SPLINE_CURVE(2,(#8464,#8465,#8466),.UNSPECIFIED.,.F.,.F.)
B_SPLINE_CURVE_WITH_KNOTS((3,3),(0.140651836354967,0.670383167684796),
 .UNSPECIFIED.)
CURVE()
GEOMETRIC_REPRESENTATION_ITEM()
RATIONAL_B_SPLINE_CURVE((1.11602540378444,1.28867513459481,1.11602540378444))
REPRESENTATION_ITEM('')
);
#27=(
BOUNDED_CURVE()
B_SPLINE_CURVE(2,(#8468,#8469,#8470),.UNSPECIFIED.,.F.,.F.)
B_SPLINE_CURVE_WITH_KNOTS((3,3),(0.140651836354967,0.670383167684795),
 .UNSPECIFIED.)
CURVE()
GEOMETRIC_REPRESENTATION_ITEM()
RATIONAL_B_SPLINE_CURVE((1.11602540378444,1.28867513459481,1.11602540378444))
REPRESENTATION_ITEM('')
);
#28=(
BOUNDED_CURVE()
B_SPLINE_CURVE(2,(#8472,#8473,#8474),.UNSPECIFIED.,.F.,.F.)
B_SPLINE_CURVE_WITH_KNOTS((3,3),(0.140651836354967,0.670383167684795),
 .UNSPECIFIED.)
CURVE()
GEOMETRIC_REPRESENTATION_ITEM()
RATIONAL_B_SPLINE_CURVE((1.11602540378444,1.28867513459482,1.11602540378444))
REPRESENTATION_ITEM('')
);
#29=(
BOUNDED_CURVE()
B_SPLINE_CURVE(2,(#8476,#8477,#8478),.UNSPECIFIED.,.F.,.F.)
B_SPLINE_CURVE_WITH_KNOTS((3,3),(0.140651836354967,0.670383167684795),
 .UNSPECIFIED.)
CURVE()
GEOMETRIC_REPRESENTATION_ITEM()
RATIONAL_B_SPLINE_CURVE((1.11602540378444,1.28867513459481,1.11602540378444))
REPRESENTATION_ITEM('')
);
#30=(
BOUNDED_CURVE()
B_SPLINE_CURVE(2,(#8479,#8480,#8481),.UNSPECIFIED.,.F.,.F.)
B_SPLINE_CURVE_WITH_KNOTS((3,3),(0.140651836354967,0.670383167684795),
 .UNSPECIFIED.)
CURVE()
GEOMETRIC_REPRESENTATION_ITEM()
RATIONAL_B_SPLINE_CURVE((1.11602540378444,1.28867513459481,1.11602540378444))
REPRESENTATION_ITEM('')
);
#272=CONICAL_SURFACE('',#5681,0.47094010767585,1.0471975511966);
#273=CONICAL_SURFACE('',#5683,0.47094010767585,1.0471975511966);
#300=SHAPE_REPRESENTATION_RELATIONSHIP('SRR','None',#9248,#328);
#328=ADVANCED_BREP_SHAPE_REPRESENTATION('',(#383),#9091);
#356=STYLED_ITEM('',(#9467),#383);
#383=MANIFOLD_SOLID_BREP('Body1',#4943);
#472=FACE_BOUND('',#1308,.T.);
#473=FACE_BOUND('',#1310,.T.);
#639=PLANE('',#5685);
#640=PLANE('',#5686);
#641=PLANE('',#5687);
#642=PLANE('',#5691);
#643=PLANE('',#5692);
#644=PLANE('',#5693);
#645=PLANE('',#5694);
#646=PLANE('',#5695);
#912=FACE_OUTER_BOUND('',#1298,.T.);
#913=FACE_OUTER_BOUND('',#1299,.T.);
#914=FACE_OUTER_BOUND('',#1300,.T.);
#915=FACE_OUTER_BOUND('',#1301,.T.);
#916=FACE_OUTER_BOUND('',#1302,.T.);
#917=FACE_OUTER_BOUND('',#1303,.T.);
#918=FACE_OUTER_BOUND('',#1304,.T.);
#919=FACE_OUTER_BOUND('',#1305,.T.);
#920=FACE_OUTER_BOUND('',#1306,.T.);
#921=FACE_OUTER_BOUND('',#1307,.T.);
#922=FACE_OUTER_BOUND('',#1309,.T.);
#1298=EDGE_LOOP('',(#4159,#4160,#4161,#4162,#4163,#4164,#4165,#4166,#4167));
#1299=EDGE_LOOP('',(#4168,#4169,#4170,#4171,#4172,#4173,#4174,#4175,#4176));
#1300=EDGE_LOOP('',(#4177,#4178,#4179,#4180));
#1301=EDGE_LOOP('',(#4181,#4182,#4183,#4184));
#1302=EDGE_LOOP('',(#4185,#4186,#4187,#4188));
#1303=EDGE_LOOP('',(#4189,#4190,#4191,#4192));
#1304=EDGE_LOOP('',(#4193,#4194,#4195,#4196));
#1305=EDGE_LOOP('',(#4197,#4198,#4199,#4200));
#1306=EDGE_LOOP('',(#4201,#4202,#4203,#4204));
#1307=EDGE_LOOP('',(#4205));
#1308=EDGE_LOOP('',(#4206));
#1309=EDGE_LOOP('',(#4207));
#1310=EDGE_LOOP('',(#4208));
#1655=LINE('',#8437,#2004);
#1656=LINE('',#8458,#2005);
#1657=LINE('',#8483,#2006);
#1658=LINE('',#8484,#2007);
#1659=LINE('',#8486,#2008);
#1660=LINE('',#8488,#2009);
#1661=LINE('',#8493,#2010);
#1662=LINE('',#8496,#2011);
#1663=LINE('',#8498,#2012);
#2004=VECTOR('',#6974,0.47094010767585);
#2005=VECTOR('',#6981,0.47094010767585);
#2006=VECTOR('',#6984,1.);
#2007=VECTOR('',#6985,1.);
#2008=VECTOR('',#6988,1.);
#2009=VECTOR('',#6991,1.);
#2010=VECTOR('',#6996,0.25);
#2011=VECTOR('',#7001,1.);
#2012=VECTOR('',#7004,1.);
#2271=CIRCLE('',#5682,0.38);
#2272=CIRCLE('',#5684,0.38);
#2273=CIRCLE('',#5689,0.2117);
#2274=CIRCLE('',#5690,0.2117);
#2595=VERTEX_POINT('',#8427);
#2596=VERTEX_POINT('',#8428);
#2597=VERTEX_POINT('',#8432);
#2598=VERTEX_POINT('',#8436);
#2599=VERTEX_POINT('',#8439);
#2600=VERTEX_POINT('',#8443);
#2601=VERTEX_POINT('',#8447);
#2602=VERTEX_POINT('',#8455);
#2603=VERTEX_POINT('',#8457);
#2604=VERTEX_POINT('',#8459);
#2605=VERTEX_POINT('',#8463);
#2606=VERTEX_POINT('',#8467);
#2607=VERTEX_POINT('',#8471);
#2608=VERTEX_POINT('',#8475);
#2609=VERTEX_POINT('',#8490);
#2610=VERTEX_POINT('',#8492);
#3134=EDGE_CURVE('',#2595,#2596,#19,.T.);
#3135=EDGE_CURVE('',#2597,#2595,#20,.T.);
#3136=EDGE_CURVE('',#2597,#2598,#1655,.T.);
#3137=EDGE_CURVE('',#2598,#2598,#2271,.T.);
#3138=EDGE_CURVE('',#2599,#2597,#21,.T.);
#3139=EDGE_CURVE('',#2600,#2599,#22,.T.);
#3140=EDGE_CURVE('',#2601,#2600,#23,.T.);
#3141=EDGE_CURVE('',#2596,#2601,#24,.T.);
#3142=EDGE_CURVE('',#2602,#2602,#2272,.T.);
#3143=EDGE_CURVE('',#2602,#2603,#1656,.T.);
#3144=EDGE_CURVE('',#2604,#2603,#25,.T.);
#3145=EDGE_CURVE('',#2605,#2604,#26,.T.);
#3146=EDGE_CURVE('',#2606,#2605,#27,.T.);
#3147=EDGE_CURVE('',#2607,#2606,#28,.T.);
#3148=EDGE_CURVE('',#2608,#2607,#29,.T.);
#3149=EDGE_CURVE('',#2603,#2608,#30,.T.);
#3150=EDGE_CURVE('',#2599,#2608,#1657,.T.);
#3151=EDGE_CURVE('',#2600,#2607,#1658,.T.);
#3152=EDGE_CURVE('',#2597,#2603,#1659,.T.);
#3153=EDGE_CURVE('',#2595,#2604,#1660,.T.);
#3154=EDGE_CURVE('',#2609,#2609,#2273,.F.);
#3155=EDGE_CURVE('',#2609,#2610,#1661,.T.);
#3156=EDGE_CURVE('',#2610,#2610,#2274,.F.);
#3157=EDGE_CURVE('',#2596,#2605,#1662,.T.);
#3158=EDGE_CURVE('',#2601,#2606,#1663,.T.);
#4159=ORIENTED_EDGE('',*,*,#3134,.F.);
#4160=ORIENTED_EDGE('',*,*,#3135,.F.);
#4161=ORIENTED_EDGE('',*,*,#3136,.T.);
#4162=ORIENTED_EDGE('',*,*,#3137,.F.);
#4163=ORIENTED_EDGE('',*,*,#3136,.F.);
#4164=ORIENTED_EDGE('',*,*,#3138,.F.);
#4165=ORIENTED_EDGE('',*,*,#3139,.F.);
#4166=ORIENTED_EDGE('',*,*,#3140,.F.);
#4167=ORIENTED_EDGE('',*,*,#3141,.F.);
#4168=ORIENTED_EDGE('',*,*,#3142,.F.);
#4169=ORIENTED_EDGE('',*,*,#3143,.T.);
#4170=ORIENTED_EDGE('',*,*,#3144,.F.);
#4171=ORIENTED_EDGE('',*,*,#3145,.F.);
#4172=ORIENTED_EDGE('',*,*,#3146,.F.);
#4173=ORIENTED_EDGE('',*,*,#3147,.F.);
#4174=ORIENTED_EDGE('',*,*,#3148,.F.);
#4175=ORIENTED_EDGE('',*,*,#3149,.F.);
#4176=ORIENTED_EDGE('',*,*,#3143,.F.);
#4177=ORIENTED_EDGE('',*,*,#3139,.T.);
#4178=ORIENTED_EDGE('',*,*,#3150,.T.);
#4179=ORIENTED_EDGE('',*,*,#3148,.T.);
#4180=ORIENTED_EDGE('',*,*,#3151,.F.);
#4181=ORIENTED_EDGE('',*,*,#3138,.T.);
#4182=ORIENTED_EDGE('',*,*,#3152,.T.);
#4183=ORIENTED_EDGE('',*,*,#3149,.T.);
#4184=ORIENTED_EDGE('',*,*,#3150,.F.);
#4185=ORIENTED_EDGE('',*,*,#3135,.T.);
#4186=ORIENTED_EDGE('',*,*,#3153,.T.);
#4187=ORIENTED_EDGE('',*,*,#3144,.T.);
#4188=ORIENTED_EDGE('',*,*,#3152,.F.);
#4189=ORIENTED_EDGE('',*,*,#3154,.F.);
#4190=ORIENTED_EDGE('',*,*,#3155,.T.);
#4191=ORIENTED_EDGE('',*,*,#3156,.T.);
#4192=ORIENTED_EDGE('',*,*,#3155,.F.);
#4193=ORIENTED_EDGE('',*,*,#3134,.T.);
#4194=ORIENTED_EDGE('',*,*,#3157,.T.);
#4195=ORIENTED_EDGE('',*,*,#3145,.T.);
#4196=ORIENTED_EDGE('',*,*,#3153,.F.);
#4197=ORIENTED_EDGE('',*,*,#3140,.T.);
#4198=ORIENTED_EDGE('',*,*,#3151,.T.);
#4199=ORIENTED_EDGE('',*,*,#3147,.T.);
#4200=ORIENTED_EDGE('',*,*,#3158,.F.);
#4201=ORIENTED_EDGE('',*,*,#3141,.T.);
#4202=ORIENTED_EDGE('',*,*,#3158,.T.);
#4203=ORIENTED_EDGE('',*,*,#3146,.T.);
#4204=ORIENTED_EDGE('',*,*,#3157,.F.);
#4205=ORIENTED_EDGE('',*,*,#3142,.T.);
#4206=ORIENTED_EDGE('',*,*,#3154,.T.);
#4207=ORIENTED_EDGE('',*,*,#3137,.T.);
#4208=ORIENTED_EDGE('',*,*,#3156,.F.);
#4597=CYLINDRICAL_SURFACE('',#5688,0.2117);
#4835=ADVANCED_FACE('',(#912),#272,.T.);
#4836=ADVANCED_FACE('',(#913),#273,.T.);
#4837=ADVANCED_FACE('',(#914),#639,.T.);
#4838=ADVANCED_FACE('',(#915),#640,.T.);
#4839=ADVANCED_FACE('',(#916),#641,.T.);
#4840=ADVANCED_FACE('',(#917),#4597,.F.);
#4841=ADVANCED_FACE('',(#918),#642,.T.);
#4842=ADVANCED_FACE('',(#919),#643,.T.);
#4843=ADVANCED_FACE('',(#920),#644,.T.);
#4844=ADVANCED_FACE('',(#921,#472),#645,.T.);
#4845=ADVANCED_FACE('',(#922,#473),#646,.F.);
#4943=CLOSED_SHELL('',(#4835,#4836,#4837,#4838,#4839,#4840,#4841,#4842,
#4843,#4844,#4845));
#5680=AXIS2_PLACEMENT_3D('',#8425,#6970,#6971);
#5681=AXIS2_PLACEMENT_3D('',#8426,#6972,#6973);
#5682=AXIS2_PLACEMENT_3D('',#8438,#6975,#6976);
#5683=AXIS2_PLACEMENT_3D('',#8454,#6977,#6978);
#5684=AXIS2_PLACEMENT_3D('',#8456,#6979,#6980);
#5685=AXIS2_PLACEMENT_3D('',#8482,#6982,#6983);
#5686=AXIS2_PLACEMENT_3D('',#8485,#6986,#6987);
#5687=AXIS2_PLACEMENT_3D('',#8487,#6989,#6990);
#5688=AXIS2_PLACEMENT_3D('',#8489,#6992,#6993);
#5689=AXIS2_PLACEMENT_3D('',#8491,#6994,#6995);
#5690=AXIS2_PLACEMENT_3D('',#8494,#6997,#6998);
#5691=AXIS2_PLACEMENT_3D('',#8495,#6999,#7000);
#5692=AXIS2_PLACEMENT_3D('',#8497,#7002,#7003);
#5693=AXIS2_PLACEMENT_3D('',#8499,#7005,#7006);
#5694=AXIS2_PLACEMENT_3D('',#8500,#7007,#7008);
#5695=AXIS2_PLACEMENT_3D('',#8501,#7009,#7010);
#6970=DIRECTION('axis',(0.,0.,1.));
#6971=DIRECTION('refdir',(1.,0.,0.));
#6972=DIRECTION('center_axis',(0.,1.,0.));
#6973=DIRECTION('ref_axis',(1.,0.,0.));
#6974=DIRECTION('',(0.866025403784439,-0.5,1.06057523872491E-16));
#6975=DIRECTION('center_axis',(0.,-1.,0.));
#6976=DIRECTION('ref_axis',(1.,0.,0.));
#6977=DIRECTION('center_axis',(0.,-1.,0.));
#6978=DIRECTION('ref_axis',(1.,0.,0.));
#6979=DIRECTION('center_axis',(0.,1.,0.));
#6980=DIRECTION('ref_axis',(1.,0.,0.));
#6981=DIRECTION('',(-0.866025403784439,-0.5,-1.06057523872491E-16));
#6982=DIRECTION('center_axis',(1.20185167898973E-16,0.,-1.));
#6983=DIRECTION('ref_axis',(-1.,0.,-1.20185167898973E-16));
#6984=DIRECTION('',(0.,1.,0.));
#6985=DIRECTION('',(0.,1.,0.));
#6986=DIRECTION('center_axis',(-0.866025403784439,0.,-0.5));
#6987=DIRECTION('ref_axis',(-0.5,0.,0.866025403784439));
#6988=DIRECTION('',(0.,1.,0.));
#6989=DIRECTION('center_axis',(-0.866025403784439,0.,0.5));
#6990=DIRECTION('ref_axis',(0.5,0.,0.866025403784439));
#6991=DIRECTION('',(0.,1.,0.));
#6992=DIRECTION('center_axis',(0.,1.,0.));
#6993=DIRECTION('ref_axis',(1.,0.,0.));
#6994=DIRECTION('center_axis',(0.,1.,0.));
#6995=DIRECTION('ref_axis',(1.,0.,0.));
#6996=DIRECTION('',(0.,-1.,0.));
#6997=DIRECTION('center_axis',(0.,1.,0.));
#6998=DIRECTION('ref_axis',(1.,0.,0.));
#6999=DIRECTION('center_axis',(-2.40370335797945E-16,0.,1.));
#7000=DIRECTION('ref_axis',(1.,0.,2.40370335797945E-16));
#7001=DIRECTION('',(0.,1.,0.));
#7002=DIRECTION('center_axis',(0.866025403784439,0.,-0.5));
#7003=DIRECTION('ref_axis',(-0.5,0.,-0.866025403784439));
#7004=DIRECTION('',(0.,1.,0.));
#7005=DIRECTION('center_axis',(0.866025403784439,0.,0.5));
#7006=DIRECTION('ref_axis',(0.5,0.,-0.866025403784439));
#7007=DIRECTION('center_axis',(0.,1.,0.));
#7008=DIRECTION('ref_axis',(1.,0.,0.));
#7009=DIRECTION('center_axis',(0.,1.,0.));
#7010=DIRECTION('ref_axis',(1.,0.,0.));
#8425=CARTESIAN_POINT('',(0.,0.,0.));
#8426=CARTESIAN_POINT('Origin',(0.,0.0525042956467857,0.));
#8427=CARTESIAN_POINT('',(-0.230940107675851,0.0472735643746089,0.4));
#8428=CARTESIAN_POINT('',(0.23094010767585,0.0472735643746089,0.4));
#8429=CARTESIAN_POINT('Ctrl Pts',(-0.230940107675851,0.0472735643746089,
0.4));
#8430=CARTESIAN_POINT('Ctrl Pts',(1.11022302462516E-16,-0.0193931022920578,
0.4));
#8431=CARTESIAN_POINT('Ctrl Pts',(0.23094010767585,0.0472735643746089,0.4));
#8432=CARTESIAN_POINT('',(-0.461880215351701,0.0472735643746089,-5.6564012731995E-17));
#8433=CARTESIAN_POINT('Ctrl Pts',(-0.461880215351701,0.0472735643746089,
-5.6564012731995E-17));
#8434=CARTESIAN_POINT('Ctrl Pts',(-0.346410161513776,-0.0193931022920579,
0.2));
#8435=CARTESIAN_POINT('Ctrl Pts',(-0.230940107675851,0.0472735643746089,
0.4));
#8436=CARTESIAN_POINT('',(-0.38,-2.08166817117217E-17,-4.65365783675994E-17));
#8437=CARTESIAN_POINT('',(-0.47094010767585,0.0525042956467857,-5.7673529545534E-17));
#8438=CARTESIAN_POINT('Origin',(0.,0.,0.));
#8439=CARTESIAN_POINT('',(-0.23094010767585,0.0472735643746089,-0.4));
#8440=CARTESIAN_POINT('Ctrl Pts',(-0.23094010767585,0.0472735643746089,
-0.4));
#8441=CARTESIAN_POINT('Ctrl Pts',(-0.346410161513775,-0.0193931022920578,
-0.2));
#8442=CARTESIAN_POINT('Ctrl Pts',(-0.461880215351701,0.0472735643746089,
-5.6564012731995E-17));
#8443=CARTESIAN_POINT('',(0.23094010767585,0.0472735643746089,-0.4));
#8444=CARTESIAN_POINT('Ctrl Pts',(0.23094010767585,0.0472735643746089,-0.4));
#8445=CARTESIAN_POINT('Ctrl Pts',(0.,-0.0193931022920578,-0.4));
#8446=CARTESIAN_POINT('Ctrl Pts',(-0.23094010767585,0.0472735643746089,
-0.4));
#8447=CARTESIAN_POINT('',(0.461880215351701,0.0472735643746089,0.));
#8448=CARTESIAN_POINT('Ctrl Pts',(0.461880215351701,0.0472735643746089,
0.));
#8449=CARTESIAN_POINT('Ctrl Pts',(0.346410161513776,-0.019393102292058,
-0.2));
#8450=CARTESIAN_POINT('Ctrl Pts',(0.23094010767585,0.0472735643746089,-0.4));
#8451=CARTESIAN_POINT('Ctrl Pts',(0.23094010767585,0.0472735643746089,0.4));
#8452=CARTESIAN_POINT('Ctrl Pts',(0.346410161513776,-0.0193931022920577,
0.2));
#8453=CARTESIAN_POINT('Ctrl Pts',(0.461880215351701,0.0472735643746089,
0.));
#8454=CARTESIAN_POINT('Origin',(0.,0.417495704353214,0.));
#8455=CARTESIAN_POINT('',(-0.38,0.47,-4.65365783675994E-17));
#8456=CARTESIAN_POINT('Origin',(0.,0.47,0.));
#8457=CARTESIAN_POINT('',(-0.461880215351701,0.422726435625391,-5.6564012731995E-17));
#8458=CARTESIAN_POINT('',(-0.47094010767585,0.417495704353214,-5.7673529545534E-17));
#8459=CARTESIAN_POINT('',(-0.230940107675851,0.422726435625391,0.4));
#8460=CARTESIAN_POINT('Ctrl Pts',(-0.230940107675851,0.422726435625391,
0.4));
#8461=CARTESIAN_POINT('Ctrl Pts',(-0.346410161513776,0.489393102292058,
0.2));
#8462=CARTESIAN_POINT('Ctrl Pts',(-0.461880215351701,0.422726435625391,
-5.6564012731995E-17));
#8463=CARTESIAN_POINT('',(0.23094010767585,0.422726435625391,0.4));
#8464=CARTESIAN_POINT('Ctrl Pts',(0.23094010767585,0.422726435625391,0.4));
#8465=CARTESIAN_POINT('Ctrl Pts',(8.32667268468867E-17,0.489393102292058,
0.4));
#8466=CARTESIAN_POINT('Ctrl Pts',(-0.230940107675851,0.422726435625391,
0.4));
#8467=CARTESIAN_POINT('',(0.461880215351701,0.422726435625391,0.));
#8468=CARTESIAN_POINT('Ctrl Pts',(0.461880215351701,0.422726435625391,0.));
#8469=CARTESIAN_POINT('Ctrl Pts',(0.346410161513776,0.489393102292058,0.2));
#8470=CARTESIAN_POINT('Ctrl Pts',(0.23094010767585,0.422726435625391,0.4));
#8471=CARTESIAN_POINT('',(0.23094010767585,0.422726435625391,-0.4));
#8472=CARTESIAN_POINT('Ctrl Pts',(0.23094010767585,0.422726435625391,-0.4));
#8473=CARTESIAN_POINT('Ctrl Pts',(0.346410161513775,0.489393102292058,-0.2));
#8474=CARTESIAN_POINT('Ctrl Pts',(0.461880215351701,0.422726435625391,0.));
#8475=CARTESIAN_POINT('',(-0.23094010767585,0.422726435625391,-0.4));
#8476=CARTESIAN_POINT('Ctrl Pts',(-0.23094010767585,0.422726435625391,-0.4));
#8477=CARTESIAN_POINT('Ctrl Pts',(-5.55111512312578E-17,0.489393102292058,
-0.4));
#8478=CARTESIAN_POINT('Ctrl Pts',(0.23094010767585,0.422726435625391,-0.4));
#8479=CARTESIAN_POINT('Ctrl Pts',(-0.461880215351701,0.422726435625391,
-5.6564012731995E-17));
#8480=CARTESIAN_POINT('Ctrl Pts',(-0.346410161513776,0.489393102292058,
-0.2));
#8481=CARTESIAN_POINT('Ctrl Pts',(-0.23094010767585,0.422726435625391,-0.4));
#8482=CARTESIAN_POINT('Origin',(0.23094010767585,0.,-0.4));
#8483=CARTESIAN_POINT('',(-0.23094010767585,0.,-0.4));
#8484=CARTESIAN_POINT('',(0.23094010767585,0.,-0.4));
#8485=CARTESIAN_POINT('Origin',(-0.23094010767585,0.,-0.4));
#8486=CARTESIAN_POINT('',(-0.461880215351701,0.,-5.6564012731995E-17));
#8487=CARTESIAN_POINT('Origin',(-0.461880215351701,0.,-5.6564012731995E-17));
#8488=CARTESIAN_POINT('',(-0.230940107675851,0.,0.4));
#8489=CARTESIAN_POINT('Origin',(0.,0.,0.));
#8490=CARTESIAN_POINT('',(-0.2117,0.47,2.59257727379495E-17));
#8491=CARTESIAN_POINT('Origin',(0.,0.47,0.));
#8492=CARTESIAN_POINT('',(-0.2117,0.,2.59257727379495E-17));
#8493=CARTESIAN_POINT('',(-0.2117,0.,2.59257727379495E-17));
#8494=CARTESIAN_POINT('Origin',(0.,0.,0.));
#8495=CARTESIAN_POINT('Origin',(-0.230940107675851,0.,0.4));
#8496=CARTESIAN_POINT('',(0.23094010767585,0.,0.4));
#8497=CARTESIAN_POINT('Origin',(0.461880215351701,0.,0.));
#8498=CARTESIAN_POINT('',(0.461880215351701,0.,0.));
#8499=CARTESIAN_POINT('Origin',(0.23094010767585,0.,0.4));
#8500=CARTESIAN_POINT('Origin',(0.,0.47,0.));
#8501=CARTESIAN_POINT('Origin',(0.,0.,0.));
#9058=UNCERTAINTY_MEASURE_WITH_UNIT(LENGTH_MEASURE(0.001),#9103,
'DISTANCE_ACCURACY_VALUE',
'Maximum model space distance between geometric entities at asserted c
onnectivities');
#9069=UNCERTAINTY_MEASURE_WITH_UNIT(LENGTH_MEASURE(0.001),#9103,
'DISTANCE_ACCURACY_VALUE',
'Maximum model space distance between geometric entities at asserted c
onnectivities');
#9091=(
GEOMETRIC_REPRESENTATION_CONTEXT(3)
GLOBAL_UNCERTAINTY_ASSIGNED_CONTEXT((#9058))
GLOBAL_UNIT_ASSIGNED_CONTEXT((#9103,#9105,#9106))
REPRESENTATION_CONTEXT('','3D')
);
#9102=(
GEOMETRIC_REPRESENTATION_CONTEXT(3)
GLOBAL_UNCERTAINTY_ASSIGNED_CONTEXT((#9069))
GLOBAL_UNIT_ASSIGNED_CONTEXT((#9103,#9105,#9106))
REPRESENTATION_CONTEXT('','3D')
);
#9103=(
LENGTH_UNIT()
NAMED_UNIT(*)
SI_UNIT(.CENTI.,.METRE.)
);
#9105=(
NAMED_UNIT(*)
PLANE_ANGLE_UNIT()
SI_UNIT($,.RADIAN.)
);
#9106=(
NAMED_UNIT(*)
SI_UNIT($,.STERADIAN.)
SOLID_ANGLE_UNIT()
);
#9128=SHAPE_DEFINITION_REPRESENTATION(#9162,#9248);
#9162=PRODUCT_DEFINITION_SHAPE('',$,#9281);
#9248=SHAPE_REPRESENTATION('',(#5680),#9091);
#9259=PRODUCT_DEFINITION_CONTEXT('part definition',#9357,'design');
#9281=PRODUCT_DEFINITION('Hex Nut - M5','Hex Nut - M5',#9313,#9259);
#9313=PRODUCT_DEFINITION_FORMATION('',$,#9380);
#9357=APPLICATION_CONTEXT(
'Core Data for Automotive Mechanical Design Process');
#9358=PRODUCT_CONTEXT('part definition',#9357,'mechanical');
#9380=PRODUCT('Hex Nut - M5','Hex Nut - M5','Hex Nut - M5',(#9358));
#9461=COLOUR_RGB('Black',0.12,0.14,0.17);
#9462=FILL_AREA_STYLE_COLOUR('',#9461);
#9463=FILL_AREA_STYLE('',(#9462));
#9464=SURFACE_STYLE_FILL_AREA(#9463);
#9465=SURFACE_SIDE_STYLE('',(#9464));
#9466=SURFACE_STYLE_USAGE(.BOTH.,#9465);
#9467=PRESENTATION_STYLE_ASSIGNMENT((#9466));
ENDSEC;
END-ISO-10303-21;
